ISO-10303-21;
HEADER;
/* Generated by software containing ST-Developer
 * from STEP Tools, Inc. (www.steptools.com) 
 */

FILE_DESCRIPTION(
/* description */ ('PAT-091'),
/* implementation_level */ '2;1');

FILE_NAME(
/* name */ 'Screw bearing cap (2).step',
/* time_stamp */ '2026-10-27T15:34:44-07:00',
/* author */ (''),
/* organization */ (''),
/* preprocessor_version */ 'ST-DEVELOPER v20.2',
/* originating_system */ 'Autodesk Translation Framework v15.17.0.0',
/* authorisation */ '');

FILE_SCHEMA (('AUTOMOTIVE_DESIGN { 1 0 10303 214 3 1 1 }'));
ENDSEC;

DATA;
#10=MECHANICAL_DESIGN_GEOMETRIC_PRESENTATION_REPRESENTATION('',(#978),#25100);
#758=SHAPE_REPRESENTATION_RELATIONSHIP('SRR','None',#25519,#868);
#868=ADVANCED_BREP_SHAPE_REPRESENTATION('',(#1102),#24989);
#978=STYLED_ITEM('',(#26198),#1102);
#1102=MANIFOLD_SOLID_BREP('Body1',#13255);
#1299=FACE_BOUND('',#3060,.T.);
#1300=FACE_BOUND('',#3064,.T.);
#1301=FACE_BOUND('',#3065,.T.);
#1302=FACE_BOUND('',#3066,.T.);
#1303=FACE_BOUND('',#3067,.T.);
#1304=FACE_BOUND('',#3068,.T.);
#1305=FACE_BOUND('',#3070,.T.);
#1306=FACE_BOUND('',#3071,.T.);
#1307=FACE_BOUND('',#3072,.T.);
#1308=FACE_BOUND('',#3073,.T.);
#1309=FACE_BOUND('',#3074,.T.);
#1684=PLANE('',#14789);
#1685=PLANE('',#14796);
#1686=PLANE('',#14797);
#2152=FACE_OUTER_BOUND('',#3054,.T.);
#2153=FACE_OUTER_BOUND('',#3055,.T.);
#2154=FACE_OUTER_BOUND('',#3056,.T.);
#2155=FACE_OUTER_BOUND('',#3057,.T.);
#2156=FACE_OUTER_BOUND('',#3058,.T.);
#2157=FACE_OUTER_BOUND('',#3059,.T.);
#2158=FACE_OUTER_BOUND('',#3061,.T.);
#2159=FACE_OUTER_BOUND('',#3062,.T.);
#2160=FACE_OUTER_BOUND('',#3063,.T.);
#2161=FACE_OUTER_BOUND('',#3069,.T.);
#3054=EDGE_LOOP('',(#9410,#9411,#9412,#9413));
#3055=EDGE_LOOP('',(#9414,#9415,#9416,#9417));
#3056=EDGE_LOOP('',(#9418,#9419,#9420,#9421));
#3057=EDGE_LOOP('',(#9422,#9423,#9424,#9425));
#3058=EDGE_LOOP('',(#9426,#9427,#9428,#9429));
#3059=EDGE_LOOP('',(#9430));
#3060=EDGE_LOOP('',(#9431));
#3061=EDGE_LOOP('',(#9432,#9433,#9434,#9435));
#3062=EDGE_LOOP('',(#9436,#9437,#9438,#9439));
#3063=EDGE_LOOP('',(#9440));
#3064=EDGE_LOOP('',(#9441));
#3065=EDGE_LOOP('',(#9442));
#3066=EDGE_LOOP('',(#9443));
#3067=EDGE_LOOP('',(#9444));
#3068=EDGE_LOOP('',(#9445));
#3069=EDGE_LOOP('',(#9446));
#3070=EDGE_LOOP('',(#9447));
#3071=EDGE_LOOP('',(#9448));
#3072=EDGE_LOOP('',(#9449));
#3073=EDGE_LOOP('',(#9450));
#3074=EDGE_LOOP('',(#9451));
#4253=LINE('',#21442,#4993);
#4254=LINE('',#21448,#4994);
#4255=LINE('',#21454,#4995);
#4256=LINE('',#21460,#4996);
#4257=LINE('',#21466,#4997);
#4258=LINE('',#21473,#4998);
#4259=LINE('',#21479,#4999);
#4993=VECTOR('',#16979,0.225);
#4994=VECTOR('',#16986,0.225);
#4995=VECTOR('',#16993,0.225);
#4996=VECTOR('',#17000,0.225);
#4997=VECTOR('',#17007,1.59);
#4998=VECTOR('',#17016,1.02);
#4999=VECTOR('',#17023,2.2);
#5694=CIRCLE('',#14775,0.225);
#5695=CIRCLE('',#14776,0.225);
#5696=CIRCLE('',#14778,0.225);
#5697=CIRCLE('',#14779,0.225);
#5698=CIRCLE('',#14781,0.225);
#5699=CIRCLE('',#14782,0.225);
#5700=CIRCLE('',#14784,0.225);
#5701=CIRCLE('',#14785,0.225);
#5702=CIRCLE('',#14787,1.59);
#5703=CIRCLE('',#14788,1.59);
#5704=CIRCLE('',#14790,1.02);
#5705=CIRCLE('',#14792,1.02);
#5706=CIRCLE('',#14794,2.2);
#5707=CIRCLE('',#14795,2.2);
#6529=VERTEX_POINT('',#21439);
#6530=VERTEX_POINT('',#21441);
#6531=VERTEX_POINT('',#21445);
#6532=VERTEX_POINT('',#21447);
#6533=VERTEX_POINT('',#21451);
#6534=VERTEX_POINT('',#21453);
#6535=VERTEX_POINT('',#21457);
#6536=VERTEX_POINT('',#21459);
#6537=VERTEX_POINT('',#21463);
#6538=VERTEX_POINT('',#21465);
#6539=VERTEX_POINT('',#21469);
#6540=VERTEX_POINT('',#21472);
#6541=VERTEX_POINT('',#21476);
#6542=VERTEX_POINT('',#21478);
#7640=EDGE_CURVE('',#6529,#6529,#5694,.T.);
#7641=EDGE_CURVE('',#6529,#6530,#4253,.T.);
#7642=EDGE_CURVE('',#6530,#6530,#5695,.T.);
#7643=EDGE_CURVE('',#6531,#6531,#5696,.T.);
#7644=EDGE_CURVE('',#6531,#6532,#4254,.T.);
#7645=EDGE_CURVE('',#6532,#6532,#5697,.T.);
#7646=EDGE_CURVE('',#6533,#6533,#5698,.T.);
#7647=EDGE_CURVE('',#6533,#6534,#4255,.T.);
#7648=EDGE_CURVE('',#6534,#6534,#5699,.T.);
#7649=EDGE_CURVE('',#6535,#6535,#5700,.T.);
#7650=EDGE_CURVE('',#6535,#6536,#4256,.T.);
#7651=EDGE_CURVE('',#6536,#6536,#5701,.T.);
#7652=EDGE_CURVE('',#6537,#6537,#5702,.T.);
#7653=EDGE_CURVE('',#6537,#6538,#4257,.T.);
#7654=EDGE_CURVE('',#6538,#6538,#5703,.T.);
#7655=EDGE_CURVE('',#6539,#6539,#5704,.T.);
#7656=EDGE_CURVE('',#6539,#6540,#4258,.T.);
#7657=EDGE_CURVE('',#6540,#6540,#5705,.T.);
#7658=EDGE_CURVE('',#6541,#6541,#5706,.T.);
#7659=EDGE_CURVE('',#6541,#6542,#4259,.T.);
#7660=EDGE_CURVE('',#6542,#6542,#5707,.T.);
#9410=ORIENTED_EDGE('',*,*,#7640,.F.);
#9411=ORIENTED_EDGE('',*,*,#7641,.T.);
#9412=ORIENTED_EDGE('',*,*,#7642,.F.);
#9413=ORIENTED_EDGE('',*,*,#7641,.F.);
#9414=ORIENTED_EDGE('',*,*,#7643,.F.);
#9415=ORIENTED_EDGE('',*,*,#7644,.T.);
#9416=ORIENTED_EDGE('',*,*,#7645,.F.);
#9417=ORIENTED_EDGE('',*,*,#7644,.F.);
#9418=ORIENTED_EDGE('',*,*,#7646,.F.);
#9419=ORIENTED_EDGE('',*,*,#7647,.T.);
#9420=ORIENTED_EDGE('',*,*,#7648,.F.);
#9421=ORIENTED_EDGE('',*,*,#7647,.F.);
#9422=ORIENTED_EDGE('',*,*,#7649,.F.);
#9423=ORIENTED_EDGE('',*,*,#7650,.T.);
#9424=ORIENTED_EDGE('',*,*,#7651,.F.);
#9425=ORIENTED_EDGE('',*,*,#7650,.F.);
#9426=ORIENTED_EDGE('',*,*,#7652,.F.);
#9427=ORIENTED_EDGE('',*,*,#7653,.T.);
#9428=ORIENTED_EDGE('',*,*,#7654,.F.);
#9429=ORIENTED_EDGE('',*,*,#7653,.F.);
#9430=ORIENTED_EDGE('',*,*,#7652,.T.);
#9431=ORIENTED_EDGE('',*,*,#7655,.T.);
#9432=ORIENTED_EDGE('',*,*,#7655,.F.);
#9433=ORIENTED_EDGE('',*,*,#7656,.T.);
#9434=ORIENTED_EDGE('',*,*,#7657,.T.);
#9435=ORIENTED_EDGE('',*,*,#7656,.F.);
#9436=ORIENTED_EDGE('',*,*,#7658,.F.);
#9437=ORIENTED_EDGE('',*,*,#7659,.T.);
#9438=ORIENTED_EDGE('',*,*,#7660,.T.);
#9439=ORIENTED_EDGE('',*,*,#7659,.F.);
#9440=ORIENTED_EDGE('',*,*,#7658,.T.);
#9441=ORIENTED_EDGE('',*,*,#7654,.T.);
#9442=ORIENTED_EDGE('',*,*,#7651,.T.);
#9443=ORIENTED_EDGE('',*,*,#7648,.T.);
#9444=ORIENTED_EDGE('',*,*,#7645,.T.);
#9445=ORIENTED_EDGE('',*,*,#7642,.T.);
#9446=ORIENTED_EDGE('',*,*,#7660,.F.);
#9447=ORIENTED_EDGE('',*,*,#7657,.F.);
#9448=ORIENTED_EDGE('',*,*,#7649,.T.);
#9449=ORIENTED_EDGE('',*,*,#7646,.T.);
#9450=ORIENTED_EDGE('',*,*,#7643,.T.);
#9451=ORIENTED_EDGE('',*,*,#7640,.T.);
#12119=CYLINDRICAL_SURFACE('',#14774,0.225);
#12120=CYLINDRICAL_SURFACE('',#14777,0.225);
#12121=CYLINDRICAL_SURFACE('',#14780,0.225);
#12122=CYLINDRICAL_SURFACE('',#14783,0.225);
#12123=CYLINDRICAL_SURFACE('',#14786,1.59);
#12124=CYLINDRICAL_SURFACE('',#14791,1.02);
#12125=CYLINDRICAL_SURFACE('',#14793,2.2);
#12519=ADVANCED_FACE('',(#2152),#12119,.F.);
#12520=ADVANCED_FACE('',(#2153),#12120,.F.);
#12521=ADVANCED_FACE('',(#2154),#12121,.F.);
#12522=ADVANCED_FACE('',(#2155),#12122,.F.);
#12523=ADVANCED_FACE('',(#2156),#12123,.T.);
#12524=ADVANCED_FACE('',(#2157,#1299),#1684,.T.);
#12525=ADVANCED_FACE('',(#2158),#12124,.F.);
#12526=ADVANCED_FACE('',(#2159),#12125,.T.);
#12527=ADVANCED_FACE('',(#2160,#1300,#1301,#1302,#1303,#1304),#1685,.T.);
#12528=ADVANCED_FACE('',(#2161,#1305,#1306,#1307,#1308,#1309),#1686,.F.);
#13255=CLOSED_SHELL('',(#12519,#12520,#12521,#12522,#12523,#12524,#12525,
#12526,#12527,#12528));
#14773=AXIS2_PLACEMENT_3D('',#21437,#16973,#16974);
#14774=AXIS2_PLACEMENT_3D('',#21438,#16975,#16976);
#14775=AXIS2_PLACEMENT_3D('',#21440,#16977,#16978);
#14776=AXIS2_PLACEMENT_3D('',#21443,#16980,#16981);
#14777=AXIS2_PLACEMENT_3D('',#21444,#16982,#16983);
#14778=AXIS2_PLACEMENT_3D('',#21446,#16984,#16985);
#14779=AXIS2_PLACEMENT_3D('',#21449,#16987,#16988);
#14780=AXIS2_PLACEMENT_3D('',#21450,#16989,#16990);
#14781=AXIS2_PLACEMENT_3D('',#21452,#16991,#16992);
#14782=AXIS2_PLACEMENT_3D('',#21455,#16994,#16995);
#14783=AXIS2_PLACEMENT_3D('',#21456,#16996,#16997);
#14784=AXIS2_PLACEMENT_3D('',#21458,#16998,#16999);
#14785=AXIS2_PLACEMENT_3D('',#21461,#17001,#17002);
#14786=AXIS2_PLACEMENT_3D('',#21462,#17003,#17004);
#14787=AXIS2_PLACEMENT_3D('',#21464,#17005,#17006);
#14788=AXIS2_PLACEMENT_3D('',#21467,#17008,#17009);
#14789=AXIS2_PLACEMENT_3D('',#21468,#17010,#17011);
#14790=AXIS2_PLACEMENT_3D('',#21470,#17012,#17013);
#14791=AXIS2_PLACEMENT_3D('',#21471,#17014,#17015);
#14792=AXIS2_PLACEMENT_3D('',#21474,#17017,#17018);
#14793=AXIS2_PLACEMENT_3D('',#21475,#17019,#17020);
#14794=AXIS2_PLACEMENT_3D('',#21477,#17021,#17022);
#14795=AXIS2_PLACEMENT_3D('',#21480,#17024,#17025);
#14796=AXIS2_PLACEMENT_3D('',#21481,#17026,#17027);
#14797=AXIS2_PLACEMENT_3D('',#21482,#17028,#17029);
#16973=DIRECTION('axis',(0.,0.,1.));
#16974=DIRECTION('refdir',(1.,0.,0.));
#16975=DIRECTION('center_axis',(1.,0.,0.));
#16976=DIRECTION('ref_axis',(0.,0.,-1.));
#16977=DIRECTION('center_axis',(1.,0.,0.));
#16978=DIRECTION('ref_axis',(0.,0.,-1.));
#16979=DIRECTION('',(1.,0.,0.));
#16980=DIRECTION('center_axis',(-1.,0.,0.));
#16981=DIRECTION('ref_axis',(0.,0.,-1.));
#16982=DIRECTION('center_axis',(1.,0.,0.));
#16983=DIRECTION('ref_axis',(0.,0.,-1.));
#16984=DIRECTION('center_axis',(1.,0.,0.));
#16985=DIRECTION('ref_axis',(0.,0.,-1.));
#16986=DIRECTION('',(1.,0.,0.));
#16987=DIRECTION('center_axis',(-1.,0.,0.));
#16988=DIRECTION('ref_axis',(0.,0.,-1.));
#16989=DIRECTION('center_axis',(1.,0.,0.));
#16990=DIRECTION('ref_axis',(0.,0.,-1.));
#16991=DIRECTION('center_axis',(1.,0.,0.));
#16992=DIRECTION('ref_axis',(0.,0.,-1.));
#16993=DIRECTION('',(1.,0.,0.));
#16994=DIRECTION('center_axis',(-1.,0.,0.));
#16995=DIRECTION('ref_axis',(0.,0.,-1.));
#16996=DIRECTION('center_axis',(1.,0.,0.));
#16997=DIRECTION('ref_axis',(0.,0.,-1.));
#16998=DIRECTION('center_axis',(1.,0.,0.));
#16999=DIRECTION('ref_axis',(0.,0.,-1.));
#17000=DIRECTION('',(1.,0.,0.));
#17001=DIRECTION('center_axis',(-1.,0.,0.));
#17002=DIRECTION('ref_axis',(0.,0.,-1.));
#17003=DIRECTION('center_axis',(1.,0.,0.));
#17004=DIRECTION('ref_axis',(0.,0.,-1.));
#17005=DIRECTION('center_axis',(1.,0.,0.));
#17006=DIRECTION('ref_axis',(0.,0.,-1.));
#17007=DIRECTION('',(-1.,0.,0.));
#17008=DIRECTION('center_axis',(-1.,0.,0.));
#17009=DIRECTION('ref_axis',(0.,0.,-1.));
#17010=DIRECTION('center_axis',(1.,0.,0.));
#17011=DIRECTION('ref_axis',(0.,0.,-1.));
#17012=DIRECTION('center_axis',(-1.,0.,0.));
#17013=DIRECTION('ref_axis',(0.,0.,-1.));
#17014=DIRECTION('center_axis',(1.,0.,0.));
#17015=DIRECTION('ref_axis',(0.,0.,-1.));
#17016=DIRECTION('',(-1.,0.,0.));
#17017=DIRECTION('center_axis',(-1.,0.,0.));
#17018=DIRECTION('ref_axis',(0.,0.,-1.));
#17019=DIRECTION('center_axis',(1.,0.,0.));
#17020=DIRECTION('ref_axis',(0.,0.,-1.));
#17021=DIRECTION('center_axis',(1.,0.,0.));
#17022=DIRECTION('ref_axis',(0.,0.,-1.));
#17023=DIRECTION('',(-1.,0.,0.));
#17024=DIRECTION('center_axis',(1.,0.,0.));
#17025=DIRECTION('ref_axis',(0.,0.,-1.));
#17026=DIRECTION('center_axis',(1.,0.,0.));
#17027=DIRECTION('ref_axis',(0.,0.,-1.));
#17028=DIRECTION('center_axis',(1.,0.,0.));
#17029=DIRECTION('ref_axis',(0.,0.,-1.));
#21437=CARTESIAN_POINT('',(0.,0.,0.));
#21438=CARTESIAN_POINT('Origin',(43.6,-1.30814754519511,4.69185245480489));
#21439=CARTESIAN_POINT('',(43.7,-1.30814754519511,4.91685245480489));
#21440=CARTESIAN_POINT('Origin',(43.7,-1.30814754519511,4.69185245480489));
#21441=CARTESIAN_POINT('',(44.,-1.30814754519511,4.91685245480489));
#21442=CARTESIAN_POINT('',(43.6,-1.30814754519511,4.91685245480489));
#21443=CARTESIAN_POINT('Origin',(44.,-1.30814754519511,4.69185245480489));
#21444=CARTESIAN_POINT('Origin',(43.6,-1.30814754519511,7.30814754519511));
#21445=CARTESIAN_POINT('',(43.7,-1.30814754519511,7.53314754519511));
#21446=CARTESIAN_POINT('Origin',(43.7,-1.30814754519511,7.30814754519511));
#21447=CARTESIAN_POINT('',(44.,-1.30814754519511,7.53314754519511));
#21448=CARTESIAN_POINT('',(43.6,-1.30814754519511,7.53314754519511));
#21449=CARTESIAN_POINT('Origin',(44.,-1.30814754519511,7.30814754519511));
#21450=CARTESIAN_POINT('Origin',(43.6,1.30814754519511,7.30814754519511));
#21451=CARTESIAN_POINT('',(43.7,1.30814754519511,7.53314754519511));
#21452=CARTESIAN_POINT('Origin',(43.7,1.30814754519511,7.30814754519511));
#21453=CARTESIAN_POINT('',(44.,1.30814754519511,7.53314754519511));
#21454=CARTESIAN_POINT('',(43.6,1.30814754519511,7.53314754519511));
#21455=CARTESIAN_POINT('Origin',(44.,1.30814754519511,7.30814754519511));
#21456=CARTESIAN_POINT('Origin',(43.6,1.30814754519511,4.69185245480489));
#21457=CARTESIAN_POINT('',(43.7,1.30814754519511,4.91685245480489));
#21458=CARTESIAN_POINT('Origin',(43.7,1.30814754519511,4.69185245480489));
#21459=CARTESIAN_POINT('',(44.,1.30814754519511,4.91685245480489));
#21460=CARTESIAN_POINT('',(43.6,1.30814754519511,4.91685245480489));
#21461=CARTESIAN_POINT('Origin',(44.,1.30814754519511,4.69185245480489));
#21462=CARTESIAN_POINT('Origin',(44.,0.,6.));
#21463=CARTESIAN_POINT('',(44.5,-1.94718841064429E-16,7.59));
#21464=CARTESIAN_POINT('Origin',(44.5,0.,6.));
#21465=CARTESIAN_POINT('',(44.,-1.94718841064429E-16,7.59));
#21466=CARTESIAN_POINT('',(44.,-1.94718841064429E-16,7.59));
#21467=CARTESIAN_POINT('Origin',(44.,0.,6.));
#21468=CARTESIAN_POINT('Origin',(44.5,0.,6.));
#21469=CARTESIAN_POINT('',(44.5,-1.2491397351303E-16,7.02));
#21470=CARTESIAN_POINT('Origin',(44.5,0.,6.));
#21471=CARTESIAN_POINT('Origin',(43.7,0.,6.));
#21472=CARTESIAN_POINT('',(43.7,-1.2491397351303E-16,7.02));
#21473=CARTESIAN_POINT('',(43.7,-1.2491397351303E-16,7.02));
#21474=CARTESIAN_POINT('Origin',(43.7,0.,6.));
#21475=CARTESIAN_POINT('Origin',(43.7,0.,6.));
#21476=CARTESIAN_POINT('',(44.,-2.69422295812418E-16,8.2));
#21477=CARTESIAN_POINT('Origin',(44.,0.,6.));
#21478=CARTESIAN_POINT('',(43.7,-2.69422295812418E-16,8.2));
#21479=CARTESIAN_POINT('',(43.7,-2.69422295812418E-16,8.2));
#21480=CARTESIAN_POINT('Origin',(43.7,0.,6.));
#21481=CARTESIAN_POINT('Origin',(44.,0.,6.));
#21482=CARTESIAN_POINT('Origin',(43.7,0.,6.));
#24868=UNCERTAINTY_MEASURE_WITH_UNIT(LENGTH_MEASURE(0.001),#25101,
'DISTANCE_ACCURACY_VALUE',
'Maximum model space distance between geometric entities at asserted c
onnectivities');
#24979=UNCERTAINTY_MEASURE_WITH_UNIT(LENGTH_MEASURE(0.001),#25101,
'DISTANCE_ACCURACY_VALUE',
'Maximum model space distance between geometric entities at asserted c
onnectivities');
#24989=(
GEOMETRIC_REPRESENTATION_CONTEXT(3)
GLOBAL_UNCERTAINTY_ASSIGNED_CONTEXT((#24868))
GLOBAL_UNIT_ASSIGNED_CONTEXT((#25101,#25103,#25104))
REPRESENTATION_CONTEXT('','3D')
);
#25100=(
GEOMETRIC_REPRESENTATION_CONTEXT(3)
GLOBAL_UNCERTAINTY_ASSIGNED_CONTEXT((#24979))
GLOBAL_UNIT_ASSIGNED_CONTEXT((#25101,#25103,#25104))
REPRESENTATION_CONTEXT('','3D')
);
#25101=(
LENGTH_UNIT()
NAMED_UNIT(*)
SI_UNIT(.CENTI.,.METRE.)
);
#25103=(
NAMED_UNIT(*)
PLANE_ANGLE_UNIT()
SI_UNIT($,.RADIAN.)
);
#25104=(
NAMED_UNIT(*)
SI_UNIT($,.STERADIAN.)
SOLID_ANGLE_UNIT()
);
#25114=SHAPE_DEFINITION_REPRESENTATION(#25234,#25519);
#25234=PRODUCT_DEFINITION_SHAPE('',$,#25640);
#25519=SHAPE_REPRESENTATION('',(#14773),#24989);
#25630=PRODUCT_DEFINITION_CONTEXT('part definition',#25992,'design');
#25640=PRODUCT_DEFINITION('Screw bearing cap (2)','Screw bearing cap (2)',
#25760,#25630);
#25760=PRODUCT_DEFINITION_FORMATION('',$,#26003);
#25992=APPLICATION_CONTEXT(
'Core Data for Automotive Mechanical Design Process');
#25993=PRODUCT_CONTEXT('part definition',#25992,'mechanical');
#26003=PRODUCT('Screw bearing cap (2)','Screw bearing cap (2)',
'Screw bearing cap (2)',(#25993));
#26192=COLOUR_RGB('Black',0.12,0.14,0.17);
#26193=FILL_AREA_STYLE_COLOUR('',#26192);
#26194=FILL_AREA_STYLE('',(#26193));
#26195=SURFACE_STYLE_FILL_AREA(#26194);
#26196=SURFACE_SIDE_STYLE('',(#26195));
#26197=SURFACE_STYLE_USAGE(.BOTH.,#26196);
#26198=PRESENTATION_STYLE_ASSIGNMENT((#26197));
ENDSEC;
END-ISO-10303-21;
